ISO-10303-21;
HEADER;
/* Generated by software containing ST-Developer
 * from STEP Tools, Inc. (www.steptools.com) 
 */

FILE_DESCRIPTION(
/* description */ ('Independent four-jaw lathe chuck,200mm body,40mm bore,36\X2\2013\X0\7
6mm nominal opposed jaw opening. Four shared machined T-jaws and model
ed partial M12x1.75 feed screws, native independent screw/slider links
, removable bolted bronze-bearing cartridges, fully captured ring/wash
er/head thrust stacks and registered bolted backplate. Custom spindle 
interface; no compatibility, speed, grip force or safety rating assign
ed.'),
/* implementation_level */ '2;1');

FILE_NAME(
/* name */ 'Thrust washer.step',
/* time_stamp */ '2026-11-09T20:24:54-08:00',
/* author */ (''),
/* organization */ (''),
/* preprocessor_version */ 'ST-DEVELOPER v20.2',
/* originating_system */ 'Autodesk Translation Framework v15.17.0.0',
/* authorisation */ '');

FILE_SCHEMA (('AUTOMOTIVE_DESIGN { 1 0 10303 214 3 1 1 }'));
ENDSEC;

DATA;
#10=MECHANICAL_DESIGN_GEOMETRIC_PRESENTATION_REPRESENTATION('',(#243),#69491);
#221=SHAPE_REPRESENTATION_RELATIONSHIP('SRR','None',#69578,#232);
#232=ADVANCED_BREP_SHAPE_REPRESENTATION('',(#254),#69487);
#243=STYLED_ITEM('',(#69642),#254);
#254=MANIFOLD_SOLID_BREP('Body1',#14738);
#357=FACE_BOUND('',#1963,.T.);
#358=FACE_BOUND('',#1965,.T.);
#498=PLANE('',#15613);
#499=PLANE('',#15614);
#1120=FACE_OUTER_BOUND('',#1960,.T.);
#1121=FACE_OUTER_BOUND('',#1961,.T.);
#1122=FACE_OUTER_BOUND('',#1962,.T.);
#1123=FACE_OUTER_BOUND('',#1964,.T.);
#1960=EDGE_LOOP('',(#12347,#12348,#12349,#12350));
#1961=EDGE_LOOP('',(#12351,#12352,#12353,#12354));
#1962=EDGE_LOOP('',(#12355));
#1963=EDGE_LOOP('',(#12356));
#1964=EDGE_LOOP('',(#12357));
#1965=EDGE_LOOP('',(#12358));
#2323=CIRCLE('',#15608,6.);
#2324=CIRCLE('',#15609,6.);
#2325=CIRCLE('',#15611,10.);
#2326=CIRCLE('',#15612,10.);
#4188=LINE('',#59282,#5036);
#4189=LINE('',#59288,#5037);
#5036=VECTOR('',#18014,6.);
#5037=VECTOR('',#18021,10.);
#6357=VERTEX_POINT('',#59279);
#6358=VERTEX_POINT('',#59281);
#6359=VERTEX_POINT('',#59285);
#6360=VERTEX_POINT('',#59287);
#8410=EDGE_CURVE('',#6357,#6357,#2323,.T.);
#8411=EDGE_CURVE('',#6357,#6358,#4188,.T.);
#8412=EDGE_CURVE('',#6358,#6358,#2324,.T.);
#8413=EDGE_CURVE('',#6359,#6359,#2325,.T.);
#8414=EDGE_CURVE('',#6359,#6360,#4189,.T.);
#8415=EDGE_CURVE('',#6360,#6360,#2326,.T.);
#12347=ORIENTED_EDGE('',*,*,#8410,.F.);
#12348=ORIENTED_EDGE('',*,*,#8411,.T.);
#12349=ORIENTED_EDGE('',*,*,#8412,.T.);
#12350=ORIENTED_EDGE('',*,*,#8411,.F.);
#12351=ORIENTED_EDGE('',*,*,#8413,.F.);
#12352=ORIENTED_EDGE('',*,*,#8414,.T.);
#12353=ORIENTED_EDGE('',*,*,#8415,.T.);
#12354=ORIENTED_EDGE('',*,*,#8414,.F.);
#12355=ORIENTED_EDGE('',*,*,#8413,.T.);
#12356=ORIENTED_EDGE('',*,*,#8410,.T.);
#12357=ORIENTED_EDGE('',*,*,#8415,.F.);
#12358=ORIENTED_EDGE('',*,*,#8412,.F.);
#13798=CYLINDRICAL_SURFACE('',#15607,6.);
#13799=CYLINDRICAL_SURFACE('',#15610,10.);
#14548=ADVANCED_FACE('',(#1120),#13798,.F.);
#14549=ADVANCED_FACE('',(#1121),#13799,.T.);
#14550=ADVANCED_FACE('',(#1122,#357),#498,.T.);
#14551=ADVANCED_FACE('',(#1123,#358),#499,.F.);
#14738=CLOSED_SHELL('',(#14548,#14549,#14550,#14551));
#15606=AXIS2_PLACEMENT_3D('',#59277,#18008,#18009);
#15607=AXIS2_PLACEMENT_3D('',#59278,#18010,#18011);
#15608=AXIS2_PLACEMENT_3D('',#59280,#18012,#18013);
#15609=AXIS2_PLACEMENT_3D('',#59283,#18015,#18016);
#15610=AXIS2_PLACEMENT_3D('',#59284,#18017,#18018);
#15611=AXIS2_PLACEMENT_3D('',#59286,#18019,#18020);
#15612=AXIS2_PLACEMENT_3D('',#59289,#18022,#18023);
#15613=AXIS2_PLACEMENT_3D('',#59290,#18024,#18025);
#15614=AXIS2_PLACEMENT_3D('',#59291,#18026,#18027);
#18008=DIRECTION('axis',(0.,0.,1.));
#18009=DIRECTION('refdir',(1.,0.,0.));
#18010=DIRECTION('center_axis',(0.,0.,1.));
#18011=DIRECTION('ref_axis',(1.,0.,0.));
#18012=DIRECTION('center_axis',(0.,0.,-1.));
#18013=DIRECTION('ref_axis',(1.,0.,0.));
#18014=DIRECTION('',(0.,0.,-1.));
#18015=DIRECTION('center_axis',(0.,0.,-1.));
#18016=DIRECTION('ref_axis',(1.,0.,0.));
#18017=DIRECTION('center_axis',(0.,0.,1.));
#18018=DIRECTION('ref_axis',(1.,0.,0.));
#18019=DIRECTION('center_axis',(0.,0.,1.));
#18020=DIRECTION('ref_axis',(1.,0.,0.));
#18021=DIRECTION('',(0.,0.,-1.));
#18022=DIRECTION('center_axis',(0.,0.,1.));
#18023=DIRECTION('ref_axis',(1.,0.,0.));
#18024=DIRECTION('center_axis',(0.,0.,1.));
#18025=DIRECTION('ref_axis',(1.,0.,0.));
#18026=DIRECTION('center_axis',(0.,0.,1.));
#18027=DIRECTION('ref_axis',(1.,0.,0.));
#59277=CARTESIAN_POINT('',(0.,0.,0.));
#59278=CARTESIAN_POINT('Origin',(0.,0.,0.));
#59279=CARTESIAN_POINT('',(-6.,-7.34788079488412E-16,2.));
#59280=CARTESIAN_POINT('Origin',(0.,0.,2.));
#59281=CARTESIAN_POINT('',(-6.,-7.34788079488412E-16,0.));
#59282=CARTESIAN_POINT('',(-6.,-7.34788079488412E-16,0.));
#59283=CARTESIAN_POINT('Origin',(0.,0.,0.));
#59284=CARTESIAN_POINT('Origin',(0.,0.,0.));
#59285=CARTESIAN_POINT('',(-10.,-1.22464679914735E-15,2.));
#59286=CARTESIAN_POINT('Origin',(0.,0.,2.));
#59287=CARTESIAN_POINT('',(-10.,-1.22464679914735E-15,0.));
#59288=CARTESIAN_POINT('',(-10.,-1.22464679914735E-15,0.));
#59289=CARTESIAN_POINT('Origin',(0.,0.,0.));
#59290=CARTESIAN_POINT('Origin',(0.,0.,2.));
#59291=CARTESIAN_POINT('Origin',(0.,0.,0.));
#69474=UNCERTAINTY_MEASURE_WITH_UNIT(LENGTH_MEASURE(0.01),#69492,
'DISTANCE_ACCURACY_VALUE',
'Maximum model space distance between geometric entities at asserted c
onnectivities');
#69478=UNCERTAINTY_MEASURE_WITH_UNIT(LENGTH_MEASURE(0.01),#69492,
'DISTANCE_ACCURACY_VALUE',
'Maximum model space distance between geometric entities at asserted c
onnectivities');
#69487=(
GEOMETRIC_REPRESENTATION_CONTEXT(3)
GLOBAL_UNCERTAINTY_ASSIGNED_CONTEXT((#69474))
GLOBAL_UNIT_ASSIGNED_CONTEXT((#69492,#69494,#69495))
REPRESENTATION_CONTEXT('','3D')
);
#69491=(
GEOMETRIC_REPRESENTATION_CONTEXT(3)
GLOBAL_UNCERTAINTY_ASSIGNED_CONTEXT((#69478))
GLOBAL_UNIT_ASSIGNED_CONTEXT((#69492,#69494,#69495))
REPRESENTATION_CONTEXT('','3D')
);
#69492=(
LENGTH_UNIT()
NAMED_UNIT(*)
SI_UNIT(.MILLI.,.METRE.)
);
#69494=(
NAMED_UNIT(*)
PLANE_ANGLE_UNIT()
SI_UNIT($,.RADIAN.)
);
#69495=(
NAMED_UNIT(*)
SI_UNIT($,.STERADIAN.)
SOLID_ANGLE_UNIT()
);
#69504=SHAPE_DEFINITION_REPRESENTATION(#69516,#69578);
#69516=PRODUCT_DEFINITION_SHAPE('',$,#69591);
#69578=SHAPE_REPRESENTATION('',(#15606),#69487);
#69582=PRODUCT_DEFINITION_CONTEXT('part definition',#69620,'design');
#69591=PRODUCT_DEFINITION('Thrust washer','Thrust washer',#69603,#69582);
#69603=PRODUCT_DEFINITION_FORMATION('',$,#69630);
#69620=APPLICATION_CONTEXT(
'Core Data for Automotive Mechanical Design Process');
#69621=PRODUCT_CONTEXT('part definition',#69620,'mechanical');
#69630=PRODUCT('Thrust washer','Thrust washer',$,(#69621));
#69642=PRESENTATION_STYLE_ASSIGNMENT((#69652));
#69652=SURFACE_STYLE_USAGE(.BOTH.,#69662);
#69662=SURFACE_SIDE_STYLE('',(#69672));
#69672=SURFACE_STYLE_FILL_AREA(#69682);
#69682=FILL_AREA_STYLE('Bearing gray',(#69692));
#69692=FILL_AREA_STYLE_COLOUR('Bearing gray',#69702);
#69702=COLOUR_RGB('Bearing gray',0.576470588235294,0.615686274509804,0.666666666666667);
ENDSEC;
END-ISO-10303-21;
